ISO-10303-21;
HEADER;
/* Generated by software containing ST-Developer
 * from STEP Tools, Inc. (www.steptools.com) 
 */

FILE_DESCRIPTION(
/* description */ (''),
/* implementation_level */ '2;1');

FILE_NAME(
/* name */ 'Nut_02.step',
/* time_stamp */ '2026-10-06T13:05:37-07:00',
/* author */ (''),
/* organization */ (''),
/* preprocessor_version */ 'ST-DEVELOPER v20.2',
/* originating_system */ 'Autodesk Translation Framework v15.15.0.0',
/* authorisation */ '');

FILE_SCHEMA (('AUTOMOTIVE_DESIGN { 1 0 10303 214 3 1 1 }'));
ENDSEC;

DATA;
#10=MECHANICAL_DESIGN_GEOMETRIC_PRESENTATION_REPRESENTATION('',(#138),#28055);
#60=B_SPLINE_SURFACE_WITH_KNOTS('',3,1,((#15514,#15515),(#15516,#15517),
(#15518,#15519),(#15520,#15521),(#15522,#15523),(#15524,#15525),(#15526,
#15527),(#15528,#15529),(#15530,#15531),(#15532,#15533),(#15534,#15535),
(#15536,#15537),(#15538,#15539),(#15540,#15541)),.UNSPECIFIED.,.F.,.F.,
 .F.,(4,2,2,2,2,2,4),(2,2),(-0.844212290556731,-0.730966332817565,-0.619975754240938,
-0.457326579004558,-0.29977928179387,-0.147336283383114,0.),(0.,0.48),
 .UNSPECIFIED.);
#61=B_SPLINE_SURFACE_WITH_KNOTS('',3,1,((#15582,#15583),(#15584,#15585),
(#15586,#15587),(#15588,#15589),(#15590,#15591),(#15592,#15593),(#15594,
#15595),(#15596,#15597),(#15598,#15599),(#15600,#15601),(#15602,#15603),
(#15604,#15605),(#15606,#15607),(#15608,#15609)),.UNSPECIFIED.,.F.,.F.,
 .F.,(4,2,2,2,2,2,4),(2,2),(-0.847325527525843,-0.749719327139836,-0.649860858750851,
-0.495073659399383,-0.335166304629316,-0.170141007879843,0.),(0.,0.48),
 .UNSPECIFIED.);
#118=SHAPE_REPRESENTATION_RELATIONSHIP('SRR','None',#28095,#128);
#128=ADVANCED_BREP_SHAPE_REPRESENTATION('',(#148),#28047);
#138=STYLED_ITEM('',(#28152),#148);
#148=MANIFOLD_SOLID_BREP('Body1',#3679);
#191=FACE_BOUND('',#689,.T.);
#192=FACE_BOUND('',#691,.T.);
#221=PLANE('',#3954);
#222=PLANE('',#3955);
#223=PLANE('',#3956);
#224=PLANE('',#3957);
#225=PLANE('',#3958);
#226=PLANE('',#3959);
#227=PLANE('',#3960);
#228=PLANE('',#3961);
#327=CIRCLE('',#3949,4.433);
#328=CIRCLE('',#3950,4.433);
#329=CIRCLE('',#3952,3.72275);
#330=CIRCLE('',#3953,3.72275);
#454=FACE_OUTER_BOUND('',#678,.T.);
#455=FACE_OUTER_BOUND('',#679,.T.);
#456=FACE_OUTER_BOUND('',#680,.T.);
#457=FACE_OUTER_BOUND('',#681,.T.);
#458=FACE_OUTER_BOUND('',#682,.T.);
#459=FACE_OUTER_BOUND('',#683,.T.);
#460=FACE_OUTER_BOUND('',#684,.T.);
#461=FACE_OUTER_BOUND('',#685,.T.);
#462=FACE_OUTER_BOUND('',#686,.T.);
#463=FACE_OUTER_BOUND('',#687,.T.);
#464=FACE_OUTER_BOUND('',#688,.T.);
#465=FACE_OUTER_BOUND('',#690,.T.);
#678=EDGE_LOOP('',(#2700,#2701,#2702,#2703));
#679=EDGE_LOOP('',(#2704,#2705,#2706,#2707));
#680=EDGE_LOOP('',(#2708,#2709,#2710,#2711));
#681=EDGE_LOOP('',(#2712,#2713,#2714,#2715));
#682=EDGE_LOOP('',(#2716,#2717,#2718,#2719));
#683=EDGE_LOOP('',(#2720,#2721,#2722,#2723));
#684=EDGE_LOOP('',(#2724,#2725,#2726,#2727));
#685=EDGE_LOOP('',(#2728,#2729,#2730,#2731));
#686=EDGE_LOOP('',(#2732,#2733,#2734,#2735));
#687=EDGE_LOOP('',(#2736,#2737,#2738,#2739));
#688=EDGE_LOOP('',(#2740,#2741,#2742,#2743,#2744,#2745));
#689=EDGE_LOOP('',(#2746,#2747,#2748,#2749));
#690=EDGE_LOOP('',(#2750,#2751,#2752,#2753,#2754,#2755));
#691=EDGE_LOOP('',(#2756,#2757,#2758,#2759));
#862=LINE('',#15559,#1020);
#863=LINE('',#15575,#1021);
#864=LINE('',#15581,#1022);
#865=LINE('',#15640,#1023);
#866=LINE('',#15647,#1024);
#867=LINE('',#15649,#1025);
#868=LINE('',#15651,#1026);
#869=LINE('',#15652,#1027);
#870=LINE('',#15655,#1028);
#871=LINE('',#15657,#1029);
#872=LINE('',#15658,#1030);
#873=LINE('',#15661,#1031);
#874=LINE('',#15663,#1032);
#875=LINE('',#15664,#1033);
#876=LINE('',#15667,#1034);
#877=LINE('',#15669,#1035);
#878=LINE('',#15670,#1036);
#879=LINE('',#15673,#1037);
#880=LINE('',#15675,#1038);
#881=LINE('',#15676,#1039);
#882=LINE('',#15678,#1040);
#883=LINE('',#15679,#1041);
#1020=VECTOR('',#4451,10.);
#1021=VECTOR('',#4452,10.);
#1022=VECTOR('',#4459,10.);
#1023=VECTOR('',#4460,10.);
#1024=VECTOR('',#4469,10.);
#1025=VECTOR('',#4470,10.);
#1026=VECTOR('',#4471,10.);
#1027=VECTOR('',#4472,10.);
#1028=VECTOR('',#4475,9.99999999999999);
#1029=VECTOR('',#4476,9.99999999999999);
#1030=VECTOR('',#4477,10.);
#1031=VECTOR('',#4480,10.);
#1032=VECTOR('',#4481,10.);
#1033=VECTOR('',#4482,10.);
#1034=VECTOR('',#4485,10.);
#1035=VECTOR('',#4486,10.);
#1036=VECTOR('',#4487,10.);
#1037=VECTOR('',#4490,10.);
#1038=VECTOR('',#4491,10.);
#1039=VECTOR('',#4492,10.);
#1040=VECTOR('',#4495,10.);
#1041=VECTOR('',#4496,10.);
#1220=B_SPLINE_CURVE_WITH_KNOTS('',3,(#15544,#15545,#15546,#15547,#15548,
#15549,#15550,#15551,#15552,#15553,#15554,#15555,#15556,#15557),
 .UNSPECIFIED.,.F.,.F.,(4,2,2,2,2,2,4),(-0.844212290556731,-0.730966332817565,
-0.619975754240938,-0.457326579004558,-0.29977928179387,-0.147336283383114,
0.),.UNSPECIFIED.);
#1221=B_SPLINE_CURVE_WITH_KNOTS('',3,(#15561,#15562,#15563,#15564,#15565,
#15566,#15567,#15568,#15569,#15570,#15571,#15572,#15573,#15574),
 .UNSPECIFIED.,.F.,.F.,(4,2,2,2,2,2,4),(-0.844212290556731,-0.730966332817565,
-0.619975754240938,-0.457326579004558,-0.29977928179387,-0.147336283383114,
0.),.UNSPECIFIED.);
#1222=B_SPLINE_CURVE_WITH_KNOTS('',3,(#15611,#15612,#15613,#15614,#15615,
#15616,#15617,#15618,#15619,#15620,#15621,#15622,#15623,#15624),
 .UNSPECIFIED.,.F.,.F.,(4,2,2,2,2,2,4),(-0.847325527525843,-0.749719327139836,
-0.649860858750851,-0.495073659399383,-0.335166304629316,-0.170141007879843,
0.),.UNSPECIFIED.);
#1223=B_SPLINE_CURVE_WITH_KNOTS('',3,(#15626,#15627,#15628,#15629,#15630,
#15631,#15632,#15633,#15634,#15635,#15636,#15637,#15638,#15639),
 .UNSPECIFIED.,.F.,.F.,(4,2,2,2,2,2,4),(-0.847325527525843,-0.749719327139836,
-0.649860858750851,-0.495073659399383,-0.335166304629316,-0.170141007879843,
0.),.UNSPECIFIED.);
#1532=VERTEX_POINT('',#15542);
#1533=VERTEX_POINT('',#15543);
#1534=VERTEX_POINT('',#15558);
#1535=VERTEX_POINT('',#15560);
#1536=VERTEX_POINT('',#15577);
#1537=VERTEX_POINT('',#15579);
#1538=VERTEX_POINT('',#15610);
#1539=VERTEX_POINT('',#15625);
#1540=VERTEX_POINT('',#15645);
#1541=VERTEX_POINT('',#15646);
#1542=VERTEX_POINT('',#15648);
#1543=VERTEX_POINT('',#15650);
#1544=VERTEX_POINT('',#15654);
#1545=VERTEX_POINT('',#15656);
#1546=VERTEX_POINT('',#15660);
#1547=VERTEX_POINT('',#15662);
#1548=VERTEX_POINT('',#15666);
#1549=VERTEX_POINT('',#15668);
#1550=VERTEX_POINT('',#15672);
#1551=VERTEX_POINT('',#15674);
#1963=EDGE_CURVE('',#1532,#1533,#1220,.T.);
#1964=EDGE_CURVE('',#1533,#1534,#862,.T.);
#1965=EDGE_CURVE('',#1535,#1534,#1221,.T.);
#1966=EDGE_CURVE('',#1532,#1535,#863,.T.);
#1967=EDGE_CURVE('',#1536,#1532,#327,.T.);
#1968=EDGE_CURVE('',#1537,#1535,#328,.T.);
#1969=EDGE_CURVE('',#1536,#1537,#864,.T.);
#1970=EDGE_CURVE('',#1538,#1536,#1222,.T.);
#1971=EDGE_CURVE('',#1539,#1537,#1223,.T.);
#1972=EDGE_CURVE('',#1538,#1539,#865,.T.);
#1973=EDGE_CURVE('',#1533,#1538,#329,.T.);
#1974=EDGE_CURVE('',#1534,#1539,#330,.T.);
#1975=EDGE_CURVE('',#1540,#1541,#866,.T.);
#1976=EDGE_CURVE('',#1541,#1542,#867,.T.);
#1977=EDGE_CURVE('',#1543,#1542,#868,.T.);
#1978=EDGE_CURVE('',#1540,#1543,#869,.T.);
#1979=EDGE_CURVE('',#1544,#1540,#870,.T.);
#1980=EDGE_CURVE('',#1545,#1543,#871,.T.);
#1981=EDGE_CURVE('',#1544,#1545,#872,.T.);
#1982=EDGE_CURVE('',#1546,#1544,#873,.T.);
#1983=EDGE_CURVE('',#1547,#1545,#874,.T.);
#1984=EDGE_CURVE('',#1546,#1547,#875,.T.);
#1985=EDGE_CURVE('',#1548,#1546,#876,.T.);
#1986=EDGE_CURVE('',#1549,#1547,#877,.T.);
#1987=EDGE_CURVE('',#1548,#1549,#878,.T.);
#1988=EDGE_CURVE('',#1550,#1548,#879,.T.);
#1989=EDGE_CURVE('',#1551,#1549,#880,.T.);
#1990=EDGE_CURVE('',#1550,#1551,#881,.T.);
#1991=EDGE_CURVE('',#1541,#1550,#882,.T.);
#1992=EDGE_CURVE('',#1542,#1551,#883,.T.);
#2700=ORIENTED_EDGE('',*,*,#1963,.T.);
#2701=ORIENTED_EDGE('',*,*,#1964,.T.);
#2702=ORIENTED_EDGE('',*,*,#1965,.F.);
#2703=ORIENTED_EDGE('',*,*,#1966,.F.);
#2704=ORIENTED_EDGE('',*,*,#1967,.T.);
#2705=ORIENTED_EDGE('',*,*,#1966,.T.);
#2706=ORIENTED_EDGE('',*,*,#1968,.F.);
#2707=ORIENTED_EDGE('',*,*,#1969,.F.);
#2708=ORIENTED_EDGE('',*,*,#1970,.T.);
#2709=ORIENTED_EDGE('',*,*,#1969,.T.);
#2710=ORIENTED_EDGE('',*,*,#1971,.F.);
#2711=ORIENTED_EDGE('',*,*,#1972,.F.);
#2712=ORIENTED_EDGE('',*,*,#1973,.T.);
#2713=ORIENTED_EDGE('',*,*,#1972,.T.);
#2714=ORIENTED_EDGE('',*,*,#1974,.F.);
#2715=ORIENTED_EDGE('',*,*,#1964,.F.);
#2716=ORIENTED_EDGE('',*,*,#1975,.T.);
#2717=ORIENTED_EDGE('',*,*,#1976,.T.);
#2718=ORIENTED_EDGE('',*,*,#1977,.F.);
#2719=ORIENTED_EDGE('',*,*,#1978,.F.);
#2720=ORIENTED_EDGE('',*,*,#1979,.T.);
#2721=ORIENTED_EDGE('',*,*,#1978,.T.);
#2722=ORIENTED_EDGE('',*,*,#1980,.F.);
#2723=ORIENTED_EDGE('',*,*,#1981,.F.);
#2724=ORIENTED_EDGE('',*,*,#1982,.T.);
#2725=ORIENTED_EDGE('',*,*,#1981,.T.);
#2726=ORIENTED_EDGE('',*,*,#1983,.F.);
#2727=ORIENTED_EDGE('',*,*,#1984,.F.);
#2728=ORIENTED_EDGE('',*,*,#1985,.T.);
#2729=ORIENTED_EDGE('',*,*,#1984,.T.);
#2730=ORIENTED_EDGE('',*,*,#1986,.F.);
#2731=ORIENTED_EDGE('',*,*,#1987,.F.);
#2732=ORIENTED_EDGE('',*,*,#1988,.T.);
#2733=ORIENTED_EDGE('',*,*,#1987,.T.);
#2734=ORIENTED_EDGE('',*,*,#1989,.F.);
#2735=ORIENTED_EDGE('',*,*,#1990,.F.);
#2736=ORIENTED_EDGE('',*,*,#1991,.T.);
#2737=ORIENTED_EDGE('',*,*,#1990,.T.);
#2738=ORIENTED_EDGE('',*,*,#1992,.F.);
#2739=ORIENTED_EDGE('',*,*,#1976,.F.);
#2740=ORIENTED_EDGE('',*,*,#1992,.T.);
#2741=ORIENTED_EDGE('',*,*,#1989,.T.);
#2742=ORIENTED_EDGE('',*,*,#1986,.T.);
#2743=ORIENTED_EDGE('',*,*,#1983,.T.);
#2744=ORIENTED_EDGE('',*,*,#1980,.T.);
#2745=ORIENTED_EDGE('',*,*,#1977,.T.);
#2746=ORIENTED_EDGE('',*,*,#1974,.T.);
#2747=ORIENTED_EDGE('',*,*,#1971,.T.);
#2748=ORIENTED_EDGE('',*,*,#1968,.T.);
#2749=ORIENTED_EDGE('',*,*,#1965,.T.);
#2750=ORIENTED_EDGE('',*,*,#1991,.F.);
#2751=ORIENTED_EDGE('',*,*,#1975,.F.);
#2752=ORIENTED_EDGE('',*,*,#1979,.F.);
#2753=ORIENTED_EDGE('',*,*,#1982,.F.);
#2754=ORIENTED_EDGE('',*,*,#1985,.F.);
#2755=ORIENTED_EDGE('',*,*,#1988,.F.);
#2756=ORIENTED_EDGE('',*,*,#1973,.F.);
#2757=ORIENTED_EDGE('',*,*,#1963,.F.);
#2758=ORIENTED_EDGE('',*,*,#1967,.F.);
#2759=ORIENTED_EDGE('',*,*,#1970,.F.);
#3423=CYLINDRICAL_SURFACE('',#3948,4.433);
#3424=CYLINDRICAL_SURFACE('',#3951,3.72275);
#3546=ADVANCED_FACE('',(#454),#60,.T.);
#3547=ADVANCED_FACE('',(#455),#3423,.F.);
#3548=ADVANCED_FACE('',(#456),#61,.T.);
#3549=ADVANCED_FACE('',(#457),#3424,.F.);
#3550=ADVANCED_FACE('',(#458),#221,.T.);
#3551=ADVANCED_FACE('',(#459),#222,.T.);
#3552=ADVANCED_FACE('',(#460),#223,.T.);
#3553=ADVANCED_FACE('',(#461),#224,.T.);
#3554=ADVANCED_FACE('',(#462),#225,.T.);
#3555=ADVANCED_FACE('',(#463),#226,.T.);
#3556=ADVANCED_FACE('',(#464,#191),#227,.T.);
#3557=ADVANCED_FACE('',(#465,#192),#228,.F.);
#3679=CLOSED_SHELL('',(#3546,#3547,#3548,#3549,#3550,#3551,#3552,#3553,
#3554,#3555,#3556,#3557));
#3947=AXIS2_PLACEMENT_3D('',#15513,#4449,#4450);
#3948=AXIS2_PLACEMENT_3D('',#15576,#4453,#4454);
#3949=AXIS2_PLACEMENT_3D('',#15578,#4455,#4456);
#3950=AXIS2_PLACEMENT_3D('',#15580,#4457,#4458);
#3951=AXIS2_PLACEMENT_3D('',#15641,#4461,#4462);
#3952=AXIS2_PLACEMENT_3D('',#15642,#4463,#4464);
#3953=AXIS2_PLACEMENT_3D('',#15643,#4465,#4466);
#3954=AXIS2_PLACEMENT_3D('',#15644,#4467,#4468);
#3955=AXIS2_PLACEMENT_3D('',#15653,#4473,#4474);
#3956=AXIS2_PLACEMENT_3D('',#15659,#4478,#4479);
#3957=AXIS2_PLACEMENT_3D('',#15665,#4483,#4484);
#3958=AXIS2_PLACEMENT_3D('',#15671,#4488,#4489);
#3959=AXIS2_PLACEMENT_3D('',#15677,#4493,#4494);
#3960=AXIS2_PLACEMENT_3D('',#15680,#4497,#4498);
#3961=AXIS2_PLACEMENT_3D('',#15681,#4499,#4500);
#4449=DIRECTION('axis',(0.,0.,1.));
#4450=DIRECTION('refdir',(1.,0.,0.));
#4451=DIRECTION('',(1.,0.,0.));
#4452=DIRECTION('',(1.,0.,0.));
#4453=DIRECTION('center_axis',(1.,0.,0.));
#4454=DIRECTION('ref_axis',(0.,0.444750988585694,0.895654262621492));
#4455=DIRECTION('center_axis',(-1.,0.,0.));
#4456=DIRECTION('ref_axis',(0.,0.444750988585694,0.895654262621492));
#4457=DIRECTION('center_axis',(-1.,0.,0.));
#4458=DIRECTION('ref_axis',(0.,0.444750988585694,0.895654262621492));
#4459=DIRECTION('',(1.,0.,0.));
#4460=DIRECTION('',(1.,0.,0.));
#4461=DIRECTION('center_axis',(1.,0.,0.));
#4462=DIRECTION('ref_axis',(0.,-0.580623944517215,-0.814171870708679));
#4463=DIRECTION('center_axis',(-1.,0.,0.));
#4464=DIRECTION('ref_axis',(0.,-0.580623944517215,-0.814171870708679));
#4465=DIRECTION('center_axis',(-1.,0.,0.));
#4466=DIRECTION('ref_axis',(0.,-0.580623944517215,-0.814171870708679));
#4467=DIRECTION('center_axis',(0.,0.866025403784439,0.5));
#4468=DIRECTION('ref_axis',(0.,-0.5,0.866025403784439));
#4469=DIRECTION('',(0.,-0.5,0.866025403784439));
#4470=DIRECTION('',(1.,0.,0.));
#4471=DIRECTION('',(0.,-0.5,0.866025403784439));
#4472=DIRECTION('',(1.,0.,0.));
#4473=DIRECTION('center_axis',(0.,0.866025403784438,-0.5));
#4474=DIRECTION('ref_axis',(0.,0.5,0.866025403784438));
#4475=DIRECTION('',(0.,0.5,0.866025403784438));
#4476=DIRECTION('',(0.,0.5,0.866025403784438));
#4477=DIRECTION('',(1.,0.,0.));
#4478=DIRECTION('center_axis',(0.,-3.02823770847138E-16,-1.));
#4479=DIRECTION('ref_axis',(0.,1.,-3.02823770847138E-16));
#4480=DIRECTION('',(0.,1.,-3.02823770847138E-16));
#4481=DIRECTION('',(0.,1.,-3.02823770847138E-16));
#4482=DIRECTION('',(1.,0.,0.));
#4483=DIRECTION('center_axis',(0.,-0.866025403784439,-0.5));
#4484=DIRECTION('ref_axis',(0.,0.5,-0.866025403784439));
#4485=DIRECTION('',(0.,0.5,-0.866025403784439));
#4486=DIRECTION('',(0.,0.5,-0.866025403784439));
#4487=DIRECTION('',(1.,0.,0.));
#4488=DIRECTION('center_axis',(0.,-0.866025403784439,0.5));
#4489=DIRECTION('ref_axis',(0.,-0.5,-0.866025403784439));
#4490=DIRECTION('',(0.,-0.5,-0.866025403784439));
#4491=DIRECTION('',(0.,-0.5,-0.866025403784439));
#4492=DIRECTION('',(1.,0.,0.));
#4493=DIRECTION('center_axis',(0.,6.05647541694275E-16,1.));
#4494=DIRECTION('ref_axis',(0.,-1.,6.05647541694275E-16));
#4495=DIRECTION('',(0.,-1.,6.05647541694275E-16));
#4496=DIRECTION('',(0.,-1.,6.05647541694275E-16));
#4497=DIRECTION('center_axis',(1.,0.,0.));
#4498=DIRECTION('ref_axis',(0.,1.,0.));
#4499=DIRECTION('center_axis',(1.,0.,0.));
#4500=DIRECTION('ref_axis',(0.,1.,0.));
#15513=CARTESIAN_POINT('',(0.,0.,0.));
#15514=CARTESIAN_POINT('Ctrl Pts',(6.4430005297901,1.97158113240038,3.97043534620107));
#15515=CARTESIAN_POINT('Ctrl Pts',(11.2430005297901,1.97158113240038,3.97043534620107));
#15516=CARTESIAN_POINT('Ctrl Pts',(6.4430005297901,2.29671111436096,3.77621792657107));
#15517=CARTESIAN_POINT('Ctrl Pts',(11.2430005297901,2.29671111436096,3.77621792657107));
#15518=CARTESIAN_POINT('Ctrl Pts',(6.4430005297901,2.59552275281558,3.54102114079632));
#15519=CARTESIAN_POINT('Ctrl Pts',(11.2430005297901,2.59552275281558,3.54102114079632));
#15520=CARTESIAN_POINT('Ctrl Pts',(6.4430005297901,3.11908576775695,3.00435277140383));
#15521=CARTESIAN_POINT('Ctrl Pts',(11.2430005297901,3.11908576775695,3.00435277140383));
#15522=CARTESIAN_POINT('Ctrl Pts',(6.4430005297901,3.34301024132503,2.70651491388494));
#15523=CARTESIAN_POINT('Ctrl Pts',(11.2430005297901,3.34301024132503,2.70651491388494));
#15524=CARTESIAN_POINT('Ctrl Pts',(6.4430005297901,3.79251211736076,1.90981794028965));
#15525=CARTESIAN_POINT('Ctrl Pts',(11.2430005297901,3.79251211736076,1.90981794028965));
#15526=CARTESIAN_POINT('Ctrl Pts',(6.4430005297901,3.96610878107774,1.3893796287376));
#15527=CARTESIAN_POINT('Ctrl Pts',(11.2430005297901,3.96610878107774,1.3893796287376));
#15528=CARTESIAN_POINT('Ctrl Pts',(6.4430005297901,4.09877879619631,0.327978495265378));
#15529=CARTESIAN_POINT('Ctrl Pts',(11.2430005297901,4.09877879619631,0.327978495265378));
#15530=CARTESIAN_POINT('Ctrl Pts',(6.4430005297901,4.06307606785725,-0.201870082003989));
#15531=CARTESIAN_POINT('Ctrl Pts',(11.2430005297901,4.06307606785725,-0.201870082003989));
#15532=CARTESIAN_POINT('Ctrl Pts',(6.4430005297901,3.79206680758235,-1.20058842967181));
#15533=CARTESIAN_POINT('Ctrl Pts',(11.2430005297901,3.79206680758235,-1.20058842967181));
#15534=CARTESIAN_POINT('Ctrl Pts',(6.4430005297901,3.56572122172907,-1.66148594501202));
#15535=CARTESIAN_POINT('Ctrl Pts',(11.2430005297901,3.56572122172907,-1.66148594501202));
#15536=CARTESIAN_POINT('Ctrl Pts',(6.4430005297901,2.95711124459234,-2.45497912282895));
#15537=CARTESIAN_POINT('Ctrl Pts',(11.2430005297901,2.95711124459234,-2.45497912282895));
#15538=CARTESIAN_POINT('Ctrl Pts',(6.4430005297901,2.58595465431403,-2.78386901588454));
#15539=CARTESIAN_POINT('Ctrl Pts',(11.2430005297901,2.58595465431403,-2.78386901588454));
#15540=CARTESIAN_POINT('Ctrl Pts',(6.4430005297901,2.16151778945146,-3.03095833168072));
#15541=CARTESIAN_POINT('Ctrl Pts',(11.2430005297901,2.16151778945146,-3.03095833168072));
#15542=CARTESIAN_POINT('',(6.4430005297901,1.97158113240038,3.97043534620107));
#15543=CARTESIAN_POINT('',(6.4430005297901,2.16151778945147,-3.03095833168073));
#15544=CARTESIAN_POINT('Ctrl Pts',(6.4430005297901,1.97158113240038,3.97043534620107));
#15545=CARTESIAN_POINT('Ctrl Pts',(6.4430005297901,2.29671111436096,3.77621792657107));
#15546=CARTESIAN_POINT('Ctrl Pts',(6.4430005297901,2.59552275281558,3.54102114079632));
#15547=CARTESIAN_POINT('Ctrl Pts',(6.4430005297901,3.11908576775695,3.00435277140383));
#15548=CARTESIAN_POINT('Ctrl Pts',(6.4430005297901,3.34301024132503,2.70651491388494));
#15549=CARTESIAN_POINT('Ctrl Pts',(6.4430005297901,3.79251211736076,1.90981794028965));
#15550=CARTESIAN_POINT('Ctrl Pts',(6.4430005297901,3.96610878107774,1.3893796287376));
#15551=CARTESIAN_POINT('Ctrl Pts',(6.4430005297901,4.09877879619631,0.327978495265378));
#15552=CARTESIAN_POINT('Ctrl Pts',(6.4430005297901,4.06307606785725,-0.201870082003989));
#15553=CARTESIAN_POINT('Ctrl Pts',(6.4430005297901,3.79206680758235,-1.20058842967181));
#15554=CARTESIAN_POINT('Ctrl Pts',(6.4430005297901,3.56572122172907,-1.66148594501202));
#15555=CARTESIAN_POINT('Ctrl Pts',(6.4430005297901,2.95711124459234,-2.45497912282895));
#15556=CARTESIAN_POINT('Ctrl Pts',(6.4430005297901,2.58595465431403,-2.78386901588454));
#15557=CARTESIAN_POINT('Ctrl Pts',(6.4430005297901,2.16151778945146,-3.03095833168072));
#15558=CARTESIAN_POINT('',(10.4430005297901,2.16151778945147,-3.03095833168073));
#15559=CARTESIAN_POINT('',(6.4430005297901,2.16151778945147,-3.03095833168073));
#15560=CARTESIAN_POINT('',(10.4430005297901,1.97158113240038,3.97043534620107));
#15561=CARTESIAN_POINT('Ctrl Pts',(10.4430005297901,1.97158113240038,3.97043534620107));
#15562=CARTESIAN_POINT('Ctrl Pts',(10.4430005297901,2.29671111436096,3.77621792657107));
#15563=CARTESIAN_POINT('Ctrl Pts',(10.4430005297901,2.59552275281558,3.54102114079632));
#15564=CARTESIAN_POINT('Ctrl Pts',(10.4430005297901,3.11908576775695,3.00435277140383));
#15565=CARTESIAN_POINT('Ctrl Pts',(10.4430005297901,3.34301024132503,2.70651491388494));
#15566=CARTESIAN_POINT('Ctrl Pts',(10.4430005297901,3.79251211736076,1.90981794028965));
#15567=CARTESIAN_POINT('Ctrl Pts',(10.4430005297901,3.96610878107774,1.3893796287376));
#15568=CARTESIAN_POINT('Ctrl Pts',(10.4430005297901,4.09877879619631,0.327978495265378));
#15569=CARTESIAN_POINT('Ctrl Pts',(10.4430005297901,4.06307606785725,-0.201870082003989));
#15570=CARTESIAN_POINT('Ctrl Pts',(10.4430005297901,3.79206680758235,-1.20058842967181));
#15571=CARTESIAN_POINT('Ctrl Pts',(10.4430005297901,3.56572122172907,-1.66148594501202));
#15572=CARTESIAN_POINT('Ctrl Pts',(10.4430005297901,2.95711124459234,-2.45497912282895));
#15573=CARTESIAN_POINT('Ctrl Pts',(10.4430005297901,2.58595465431403,-2.78386901588454));
#15574=CARTESIAN_POINT('Ctrl Pts',(10.4430005297901,2.16151778945146,-3.03095833168072));
#15575=CARTESIAN_POINT('',(6.4430005297901,1.97158113240038,3.97043534620107));
#15576=CARTESIAN_POINT('Origin',(6.4430005297901,-2.77555756156289E-16,
5.55111512312578E-16));
#15577=CARTESIAN_POINT('',(6.4430005297901,-1.97158113240039,3.97043534620107));
#15578=CARTESIAN_POINT('Origin',(6.4430005297901,-2.77555756156289E-16,
5.55111512312578E-16));
#15579=CARTESIAN_POINT('',(10.4430005297901,-1.97158113240039,3.97043534620107));
#15580=CARTESIAN_POINT('Origin',(10.4430005297901,-2.77555756156289E-16,
5.55111512312578E-16));
#15581=CARTESIAN_POINT('',(6.4430005297901,-1.97158113240039,3.97043534620107));
#15582=CARTESIAN_POINT('Ctrl Pts',(6.4430005297901,-2.16151778945139,-3.03095833168078));
#15583=CARTESIAN_POINT('Ctrl Pts',(11.2430005297901,-2.16151778945139,-3.03095833168078));
#15584=CARTESIAN_POINT('Ctrl Pts',(6.4430005297901,-2.4417969811413,-2.86779155838698));
#15585=CARTESIAN_POINT('Ctrl Pts',(11.2430005297901,-2.4417969811413,-2.86779155838698));
#15586=CARTESIAN_POINT('Ctrl Pts',(6.4430005297901,-2.69946597133354,-2.66855779259647));
#15587=CARTESIAN_POINT('Ctrl Pts',(11.2430005297901,-2.69946597133354,-2.66855779259647));
#15588=CARTESIAN_POINT('Ctrl Pts',(6.4430005297901,-3.16313807023027,-2.20413689736136));
#15589=CARTESIAN_POINT('Ctrl Pts',(11.2430005297901,-3.16313807023027,-2.20413689736136));
#15590=CARTESIAN_POINT('Ctrl Pts',(6.4430005297901,-3.36582061002206,-1.93954623621156));
#15591=CARTESIAN_POINT('Ctrl Pts',(11.2430005297901,-3.36582061002206,-1.93954623621156));
#15592=CARTESIAN_POINT('Ctrl Pts',(6.4430005297901,-3.7905877946382,-1.20735040930033));
#15593=CARTESIAN_POINT('Ctrl Pts',(11.2430005297901,-3.7905877946382,-1.20735040930033));
#15594=CARTESIAN_POINT('Ctrl Pts',(6.4430005297901,-3.95787261855977,-0.715467908482556));
#15595=CARTESIAN_POINT('Ctrl Pts',(11.2430005297901,-3.95787261855977,-0.715467908482556));
#15596=CARTESIAN_POINT('Ctrl Pts',(6.4430005297901,-4.0999785741866,0.321696095215354));
#15597=CARTESIAN_POINT('Ctrl Pts',(11.2430005297901,-4.0999785741866,0.321696095215354));
#15598=CARTESIAN_POINT('Ctrl Pts',(6.4430005297901,-4.06691955087291,0.857794436836504));
#15599=CARTESIAN_POINT('Ctrl Pts',(11.2430005297901,-4.06691955087291,0.857794436836504));
#15600=CARTESIAN_POINT('Ctrl Pts',(6.4430005297901,-3.79581350913489,1.90493582172488));
#15601=CARTESIAN_POINT('Ctrl Pts',(11.2430005297901,-3.79581350913489,1.90493582172488));
#15602=CARTESIAN_POINT('Ctrl Pts',(6.4430005297901,-3.55404702294629,2.40416273654669));
#15603=CARTESIAN_POINT('Ctrl Pts',(11.2430005297901,-3.55404702294629,2.40416273654669));
#15604=CARTESIAN_POINT('Ctrl Pts',(6.4430005297901,-2.88474862400959,3.29779955123577));
#15605=CARTESIAN_POINT('Ctrl Pts',(11.2430005297901,-2.88474862400959,3.29779955123577));
#15606=CARTESIAN_POINT('Ctrl Pts',(6.4430005297901,-2.45846445810197,3.67959405679302));
#15607=CARTESIAN_POINT('Ctrl Pts',(11.2430005297901,-2.45846445810197,3.67959405679302));
#15608=CARTESIAN_POINT('Ctrl Pts',(6.4430005297901,-1.9715811324004,3.97043534620107));
#15609=CARTESIAN_POINT('Ctrl Pts',(11.2430005297901,-1.9715811324004,3.97043534620107));
#15610=CARTESIAN_POINT('',(6.4430005297901,-2.16151778945139,-3.03095833168078));
#15611=CARTESIAN_POINT('Ctrl Pts',(6.4430005297901,-2.16151778945139,-3.03095833168078));
#15612=CARTESIAN_POINT('Ctrl Pts',(6.4430005297901,-2.4417969811413,-2.86779155838698));
#15613=CARTESIAN_POINT('Ctrl Pts',(6.4430005297901,-2.69946597133354,-2.66855779259647));
#15614=CARTESIAN_POINT('Ctrl Pts',(6.4430005297901,-3.16313807023027,-2.20413689736136));
#15615=CARTESIAN_POINT('Ctrl Pts',(6.4430005297901,-3.36582061002206,-1.93954623621156));
#15616=CARTESIAN_POINT('Ctrl Pts',(6.4430005297901,-3.7905877946382,-1.20735040930033));
#15617=CARTESIAN_POINT('Ctrl Pts',(6.4430005297901,-3.95787261855977,-0.715467908482556));
#15618=CARTESIAN_POINT('Ctrl Pts',(6.4430005297901,-4.0999785741866,0.321696095215354));
#15619=CARTESIAN_POINT('Ctrl Pts',(6.4430005297901,-4.06691955087291,0.857794436836504));
#15620=CARTESIAN_POINT('Ctrl Pts',(6.4430005297901,-3.79581350913489,1.90493582172488));
#15621=CARTESIAN_POINT('Ctrl Pts',(6.4430005297901,-3.55404702294629,2.40416273654669));
#15622=CARTESIAN_POINT('Ctrl Pts',(6.4430005297901,-2.88474862400959,3.29779955123577));
#15623=CARTESIAN_POINT('Ctrl Pts',(6.4430005297901,-2.45846445810197,3.67959405679302));
#15624=CARTESIAN_POINT('Ctrl Pts',(6.4430005297901,-1.9715811324004,3.97043534620107));
#15625=CARTESIAN_POINT('',(10.4430005297901,-2.16151778945139,-3.03095833168078));
#15626=CARTESIAN_POINT('Ctrl Pts',(10.4430005297901,-2.16151778945139,-3.03095833168078));
#15627=CARTESIAN_POINT('Ctrl Pts',(10.4430005297901,-2.4417969811413,-2.86779155838698));
#15628=CARTESIAN_POINT('Ctrl Pts',(10.4430005297901,-2.69946597133354,-2.66855779259647));
#15629=CARTESIAN_POINT('Ctrl Pts',(10.4430005297901,-3.16313807023027,-2.20413689736136));
#15630=CARTESIAN_POINT('Ctrl Pts',(10.4430005297901,-3.36582061002206,-1.93954623621156));
#15631=CARTESIAN_POINT('Ctrl Pts',(10.4430005297901,-3.7905877946382,-1.20735040930033));
#15632=CARTESIAN_POINT('Ctrl Pts',(10.4430005297901,-3.95787261855977,-0.715467908482556));
#15633=CARTESIAN_POINT('Ctrl Pts',(10.4430005297901,-4.0999785741866,0.321696095215354));
#15634=CARTESIAN_POINT('Ctrl Pts',(10.4430005297901,-4.06691955087291,0.857794436836504));
#15635=CARTESIAN_POINT('Ctrl Pts',(10.4430005297901,-3.79581350913489,1.90493582172488));
#15636=CARTESIAN_POINT('Ctrl Pts',(10.4430005297901,-3.55404702294629,2.40416273654669));
#15637=CARTESIAN_POINT('Ctrl Pts',(10.4430005297901,-2.88474862400959,3.29779955123577));
#15638=CARTESIAN_POINT('Ctrl Pts',(10.4430005297901,-2.45846445810197,3.67959405679302));
#15639=CARTESIAN_POINT('Ctrl Pts',(10.4430005297901,-1.9715811324004,3.97043534620107));
#15640=CARTESIAN_POINT('',(6.4430005297901,-2.16151778945139,-3.03095833168078));
#15641=CARTESIAN_POINT('Origin',(6.4430005297901,-2.77555756156289E-16,
5.55111512312578E-16));
#15642=CARTESIAN_POINT('Origin',(6.4430005297901,-2.77555756156289E-16,
5.55111512312578E-16));
#15643=CARTESIAN_POINT('Origin',(10.4430005297901,-2.77555756156289E-16,
5.55111512312578E-16));
#15644=CARTESIAN_POINT('Origin',(6.4430005297901,7.33246945257534,-3.33066907387547E-15));
#15645=CARTESIAN_POINT('',(6.4430005297901,7.33246945257534,-3.33066907387547E-15));
#15646=CARTESIAN_POINT('',(6.4430005297901,3.66623472628768,6.35010481840362));
#15647=CARTESIAN_POINT('',(6.4430005297901,7.33246945257534,-3.33066907387547E-15));
#15648=CARTESIAN_POINT('',(10.4430005297901,3.66623472628768,6.35010481840362));
#15649=CARTESIAN_POINT('',(6.4430005297901,3.66623472628768,6.35010481840362));
#15650=CARTESIAN_POINT('',(10.4430005297901,7.33246945257534,-3.33066907387547E-15));
#15651=CARTESIAN_POINT('',(10.4430005297901,7.33246945257534,-3.33066907387547E-15));
#15652=CARTESIAN_POINT('',(6.4430005297901,7.33246945257534,-3.33066907387547E-15));
#15653=CARTESIAN_POINT('Origin',(6.4430005297901,3.66623472628767,-6.35010481840363));
#15654=CARTESIAN_POINT('',(6.4430005297901,3.66623472628767,-6.35010481840363));
#15655=CARTESIAN_POINT('',(6.4430005297901,3.66623472628767,-6.35010481840363));
#15656=CARTESIAN_POINT('',(10.4430005297901,3.66623472628767,-6.35010481840363));
#15657=CARTESIAN_POINT('',(10.4430005297901,3.66623472628767,-6.35010481840363));
#15658=CARTESIAN_POINT('',(6.4430005297901,3.66623472628767,-6.35010481840363));
#15659=CARTESIAN_POINT('Origin',(6.4430005297901,-3.66623472628767,-6.35010481840362));
#15660=CARTESIAN_POINT('',(6.4430005297901,-3.66623472628767,-6.35010481840362));
#15661=CARTESIAN_POINT('',(6.4430005297901,-3.66623472628767,-6.35010481840362));
#15662=CARTESIAN_POINT('',(10.4430005297901,-3.66623472628767,-6.35010481840362));
#15663=CARTESIAN_POINT('',(10.4430005297901,-3.66623472628767,-6.35010481840362));
#15664=CARTESIAN_POINT('',(6.4430005297901,-3.66623472628767,-6.35010481840362));
#15665=CARTESIAN_POINT('Origin',(6.4430005297901,-7.33246945257535,2.77555756156289E-15));
#15666=CARTESIAN_POINT('',(6.4430005297901,-7.33246945257535,2.77555756156289E-15));
#15667=CARTESIAN_POINT('',(6.4430005297901,-7.33246945257535,2.77555756156289E-15));
#15668=CARTESIAN_POINT('',(10.4430005297901,-7.33246945257535,2.77555756156289E-15));
#15669=CARTESIAN_POINT('',(10.4430005297901,-7.33246945257535,2.77555756156289E-15));
#15670=CARTESIAN_POINT('',(6.4430005297901,-7.33246945257535,2.77555756156289E-15));
#15671=CARTESIAN_POINT('Origin',(6.4430005297901,-3.66623472628767,6.35010481840363));
#15672=CARTESIAN_POINT('',(6.4430005297901,-3.66623472628767,6.35010481840363));
#15673=CARTESIAN_POINT('',(6.4430005297901,-3.66623472628767,6.35010481840363));
#15674=CARTESIAN_POINT('',(10.4430005297901,-3.66623472628767,6.35010481840363));
#15675=CARTESIAN_POINT('',(10.4430005297901,-3.66623472628767,6.35010481840363));
#15676=CARTESIAN_POINT('',(6.4430005297901,-3.66623472628767,6.35010481840363));
#15677=CARTESIAN_POINT('Origin',(6.4430005297901,3.66623472628768,6.35010481840362));
#15678=CARTESIAN_POINT('',(6.4430005297901,3.66623472628768,6.35010481840362));
#15679=CARTESIAN_POINT('',(10.4430005297901,3.66623472628768,6.35010481840362));
#15680=CARTESIAN_POINT('Origin',(10.4430005297901,0.,0.));
#15681=CARTESIAN_POINT('Origin',(6.4430005297901,0.,0.));
#28035=UNCERTAINTY_MEASURE_WITH_UNIT(LENGTH_MEASURE(0.01),#28056,
'DISTANCE_ACCURACY_VALUE',
'Maximum model space distance between geometric entities at asserted c
onnectivities');
#28043=UNCERTAINTY_MEASURE_WITH_UNIT(LENGTH_MEASURE(0.01),#28056,
'DISTANCE_ACCURACY_VALUE',
'Maximum model space distance between geometric entities at asserted c
onnectivities');
#28047=(
GEOMETRIC_REPRESENTATION_CONTEXT(3)
GLOBAL_UNCERTAINTY_ASSIGNED_CONTEXT((#28035))
GLOBAL_UNIT_ASSIGNED_CONTEXT((#28056,#28058,#28059))
REPRESENTATION_CONTEXT('','3D')
);
#28055=(
GEOMETRIC_REPRESENTATION_CONTEXT(3)
GLOBAL_UNCERTAINTY_ASSIGNED_CONTEXT((#28043))
GLOBAL_UNIT_ASSIGNED_CONTEXT((#28056,#28058,#28059))
REPRESENTATION_CONTEXT('','3D')
);
#28056=(
LENGTH_UNIT()
NAMED_UNIT(*)
SI_UNIT(.MILLI.,.METRE.)
);
#28058=(
NAMED_UNIT(*)
PLANE_ANGLE_UNIT()
SI_UNIT($,.RADIAN.)
);
#28059=(
NAMED_UNIT(*)
SI_UNIT($,.STERADIAN.)
SOLID_ANGLE_UNIT()
);
#28063=SHAPE_DEFINITION_REPRESENTATION(#28074,#28095);
#28074=PRODUCT_DEFINITION_SHAPE('',$,#28107);
#28095=SHAPE_REPRESENTATION('',(#3947),#28047);
#28103=PRODUCT_DEFINITION_CONTEXT('part definition',#28138,'design');
#28107=PRODUCT_DEFINITION('Nut_02','Nut_02',#28118,#28103);
#28118=PRODUCT_DEFINITION_FORMATION('',$,#28143);
#28138=APPLICATION_CONTEXT(
'Core Data for Automotive Mechanical Design Process');
#28139=PRODUCT_CONTEXT('part definition',#28138,'mechanical');
#28143=PRODUCT('Nut_02','Nut_02',$,(#28139));
#28152=PRESENTATION_STYLE_ASSIGNMENT((#28155));
#28155=SURFACE_STYLE_USAGE(.BOTH.,#28158);
#28158=SURFACE_SIDE_STYLE('',(#28161));
#28161=SURFACE_STYLE_FILL_AREA(#28164);
#28164=FILL_AREA_STYLE('Opaque(160,160,160)',(#28167));
#28167=FILL_AREA_STYLE_COLOUR('Opaque(160,160,160)',#28170);
#28170=COLOUR_RGB('Opaque(160,160,160)', 0.66274510, 0.83137255, 0.94901961);
ENDSEC;
END-ISO-10303-21;
